ISO-10303-21;
HEADER;
FILE_DESCRIPTION((''),'2;1');
FILE_NAME('GEARBOX_MOUNT_NUT_M12.step','2026-10-01T22:06:14-07:00',(''),(''),'','','');
FILE_SCHEMA (('AUTOMOTIVE_DESIGN { 1 0 10303 214 3 1 1 }'));
ENDSEC;
DATA;
#10=MECHANICAL_DESIGN_GEOMETRIC_PRESENTATION_REPRESENTATION('',(#1031),#50440);
#930=SHAPE_REPRESENTATION_RELATIONSHIP('SRR','None',#50665,#975) ;
#975=ADVANCED_BREP_SHAPE_REPRESENTATION('',(#1084),#50434) ;
#1031=STYLED_ITEM('',(#50883),#1084) ;
#1084=MANIFOLD_SOLID_BREP('GEARBOX_MOUNT_NUT_M12',#28709) ;
#1401=FACE_BOUND('',#5676,.T.) ;
#1402=FACE_BOUND('',#5682,.T.) ;
#2306=PLANE('',#32224) ;
#2307=PLANE('',#32225) ;
#2308=PLANE('',#32226) ;
#2309=PLANE('',#32227) ;
#2310=PLANE('',#32228) ;
#2311=PLANE('',#32229) ;
#2312=PLANE('',#32230) ;
#2313=PLANE('',#32231) ;
#3829=FACE_OUTER_BOUND('',#5672,.T.) ;
#3830=FACE_OUTER_BOUND('',#5673,.T.) ;
#3831=FACE_OUTER_BOUND('',#5674,.T.) ;
#3832=FACE_OUTER_BOUND('',#5675,.T.) ;
#3833=FACE_OUTER_BOUND('',#5677,.T.) ;
#3834=FACE_OUTER_BOUND('',#5678,.T.) ;
#3835=FACE_OUTER_BOUND('',#5679,.T.) ;
#3836=FACE_OUTER_BOUND('',#5680,.T.) ;
#3837=FACE_OUTER_BOUND('',#5681,.T.) ;
#5672=EDGE_LOOP('',(#26349,#26350,#26351,#26352)) ;
#5673=EDGE_LOOP('',(#26353,#26354,#26355,#26356)) ;
#5674=EDGE_LOOP('',(#26357,#26358,#26359,#26360)) ;
#5675=EDGE_LOOP('',(#26361,#26362,#26363,#26364,#26365,#26366)) ;
#5676=EDGE_LOOP('',(#26367)) ;
#5677=EDGE_LOOP('',(#26368,#26369,#26370,#26371)) ;
#5678=EDGE_LOOP('',(#26372,#26373,#26374,#26375)) ;
#5679=EDGE_LOOP('',(#26376,#26377,#26378,#26379)) ;
#5680=EDGE_LOOP('',(#26380,#26381,#26382,#26383)) ;
#5681=EDGE_LOOP('',(#26384,#26385,#26386,#26387,#26388,#26389)) ;
#5682=EDGE_LOOP('',(#26390)) ;
#8142=LINE('',#49950,#10614) ;
#8143=LINE('',#49955,#10615) ;
#8144=LINE('',#49957,#10616) ;
#8145=LINE('',#49959,#10617) ;
#8146=LINE('',#49960,#10618) ;
#8147=LINE('',#49964,#10619) ;
#8148=LINE('',#49966,#10620) ;
#8149=LINE('',#49968,#10621) ;
#8150=LINE('',#49969,#10622) ;
#8151=LINE('',#49972,#10623) ;
#8152=LINE('',#49973,#10624) ;
#8153=LINE('',#49975,#10625) ;
#8154=LINE('',#49976,#10626) ;
#8155=LINE('',#49979,#10627) ;
#8156=LINE('',#49980,#10628) ;
#8157=LINE('',#49983,#10629) ;
#8158=LINE('',#49984,#10630) ;
#8159=LINE('',#49986,#10631) ;
#8160=LINE('',#49988,#10632) ;
#10614=VECTOR('',#40813,0.6) ;
#10615=VECTOR('',#40818,1.) ;
#10616=VECTOR('',#40819,1.) ;
#10617=VECTOR('',#40820,1.) ;
#10618=VECTOR('',#40821,1.) ;
#10619=VECTOR('',#40824,1.) ;
#10620=VECTOR('',#40825,1.) ;
#10621=VECTOR('',#40826,1.) ;
#10622=VECTOR('',#40827,1.) ;
#10623=VECTOR('',#40830,1.) ;
#10624=VECTOR('',#40831,1.) ;
#10625=VECTOR('',#40832,1.) ;
#10626=VECTOR('',#40833,1.) ;
#10627=VECTOR('',#40836,1.) ;
#10628=VECTOR('',#40837,1.) ;
#10629=VECTOR('',#40840,1.) ;
#10630=VECTOR('',#40841,1.) ;
#10631=VECTOR('',#40844,1.) ;
#10632=VECTOR('',#40847,1.) ;
#11804=CIRCLE('',#32222,0.6) ;
#11805=CIRCLE('',#32223,0.6) ;
#14462=VERTEX_POINT('',#49947) ;
#14463=VERTEX_POINT('',#49949) ;
#14464=VERTEX_POINT('',#49953) ;
#14465=VERTEX_POINT('',#49954) ;
#14466=VERTEX_POINT('',#49956) ;
#14467=VERTEX_POINT('',#49958) ;
#14468=VERTEX_POINT('',#49962) ;
#14469=VERTEX_POINT('',#49963) ;
#14470=VERTEX_POINT('',#49965) ;
#14471=VERTEX_POINT('',#49967) ;
#14472=VERTEX_POINT('',#49971) ;
#14473=VERTEX_POINT('',#49974) ;
#14474=VERTEX_POINT('',#49978) ;
#14475=VERTEX_POINT('',#49982) ;
#18440=EDGE_CURVE('',#14462,#14462,#11804,.T.) ;
#18441=EDGE_CURVE('',#14462,#14463,#8142,.T.) ;
#18442=EDGE_CURVE('',#14463,#14463,#11805,.T.) ;
#18443=EDGE_CURVE('',#14464,#14465,#8143,.T.) ;
#18444=EDGE_CURVE('',#14464,#14466,#8144,.T.) ;
#18445=EDGE_CURVE('',#14467,#14466,#8145,.T.) ;
#18446=EDGE_CURVE('',#14467,#14465,#8146,.T.) ;
#18447=EDGE_CURVE('',#14468,#14469,#8147,.T.) ;
#18448=EDGE_CURVE('',#14468,#14470,#8148,.T.) ;
#18449=EDGE_CURVE('',#14471,#14470,#8149,.T.) ;
#18450=EDGE_CURVE('',#14471,#14469,#8150,.T.) ;
#18451=EDGE_CURVE('',#14472,#14464,#8151,.T.) ;
#18452=EDGE_CURVE('',#14470,#14472,#8152,.T.) ;
#18453=EDGE_CURVE('',#14473,#14468,#8153,.T.) ;
#18454=EDGE_CURVE('',#14466,#14473,#8154,.T.) ;
#18455=EDGE_CURVE('',#14472,#14474,#8155,.T.) ;
#18456=EDGE_CURVE('',#14465,#14474,#8156,.T.) ;
#18457=EDGE_CURVE('',#14473,#14475,#8157,.T.) ;
#18458=EDGE_CURVE('',#14469,#14475,#8158,.T.) ;
#18459=EDGE_CURVE('',#14474,#14471,#8159,.T.) ;
#18460=EDGE_CURVE('',#14475,#14467,#8160,.T.) ;
#26349=ORIENTED_EDGE('',*,*,#18440,.F.) ;
#26350=ORIENTED_EDGE('',*,*,#18441,.T.) ;
#26351=ORIENTED_EDGE('',*,*,#18442,.F.) ;
#26352=ORIENTED_EDGE('',*,*,#18441,.F.) ;
#26353=ORIENTED_EDGE('',*,*,#18443,.F.) ;
#26354=ORIENTED_EDGE('',*,*,#18444,.T.) ;
#26355=ORIENTED_EDGE('',*,*,#18445,.F.) ;
#26356=ORIENTED_EDGE('',*,*,#18446,.T.) ;
#26357=ORIENTED_EDGE('',*,*,#18447,.F.) ;
#26358=ORIENTED_EDGE('',*,*,#18448,.T.) ;
#26359=ORIENTED_EDGE('',*,*,#18449,.F.) ;
#26360=ORIENTED_EDGE('',*,*,#18450,.T.) ;
#26361=ORIENTED_EDGE('',*,*,#18444,.F.) ;
#26362=ORIENTED_EDGE('',*,*,#18451,.F.) ;
#26363=ORIENTED_EDGE('',*,*,#18452,.F.) ;
#26364=ORIENTED_EDGE('',*,*,#18448,.F.) ;
#26365=ORIENTED_EDGE('',*,*,#18453,.F.) ;
#26366=ORIENTED_EDGE('',*,*,#18454,.F.) ;
#26367=ORIENTED_EDGE('',*,*,#18440,.T.) ;
#26368=ORIENTED_EDGE('',*,*,#18455,.F.) ;
#26369=ORIENTED_EDGE('',*,*,#18451,.T.) ;
#26370=ORIENTED_EDGE('',*,*,#18443,.T.) ;
#26371=ORIENTED_EDGE('',*,*,#18456,.T.) ;
#26372=ORIENTED_EDGE('',*,*,#18457,.F.) ;
#26373=ORIENTED_EDGE('',*,*,#18453,.T.) ;
#26374=ORIENTED_EDGE('',*,*,#18447,.T.) ;
#26375=ORIENTED_EDGE('',*,*,#18458,.T.) ;
#26376=ORIENTED_EDGE('',*,*,#18455,.T.) ;
#26377=ORIENTED_EDGE('',*,*,#18459,.T.) ;
#26378=ORIENTED_EDGE('',*,*,#18449,.T.) ;
#26379=ORIENTED_EDGE('',*,*,#18452,.T.) ;
#26380=ORIENTED_EDGE('',*,*,#18445,.T.) ;
#26381=ORIENTED_EDGE('',*,*,#18454,.T.) ;
#26382=ORIENTED_EDGE('',*,*,#18457,.T.) ;
#26383=ORIENTED_EDGE('',*,*,#18460,.T.) ;
#26384=ORIENTED_EDGE('',*,*,#18446,.F.) ;
#26385=ORIENTED_EDGE('',*,*,#18460,.F.) ;
#26386=ORIENTED_EDGE('',*,*,#18458,.F.) ;
#26387=ORIENTED_EDGE('',*,*,#18450,.F.) ;
#26388=ORIENTED_EDGE('',*,*,#18459,.F.) ;
#26389=ORIENTED_EDGE('',*,*,#18456,.F.) ;
#26390=ORIENTED_EDGE('',*,*,#18442,.T.) ;
#27055=CYLINDRICAL_SURFACE('',#32221,0.6) ;
#28564=ADVANCED_FACE('',(#3829),#27055,.F.) ;
#28565=ADVANCED_FACE('',(#3830),#2306,.F.) ;
#28566=ADVANCED_FACE('',(#3831),#2307,.F.) ;
#28567=ADVANCED_FACE('',(#3832,#1401),#2308,.T.) ;
#28568=ADVANCED_FACE('',(#3833),#2309,.F.) ;
#28569=ADVANCED_FACE('',(#3834),#2310,.F.) ;
#28570=ADVANCED_FACE('',(#3835),#2311,.F.) ;
#28571=ADVANCED_FACE('',(#3836),#2312,.F.) ;
#28572=ADVANCED_FACE('',(#3837,#1402),#2313,.T.) ;
#28709=CLOSED_SHELL('',(#28564,#28565,#28566,#28567,#28568,#28569,#28570,
#28571,#28572)) ;
#32220=AXIS2_PLACEMENT_3D('',#49945,#40807,#40808) ;
#32221=AXIS2_PLACEMENT_3D('',#49946,#40809,#40810) ;
#32222=AXIS2_PLACEMENT_3D('',#49948,#40811,#40812) ;
#32223=AXIS2_PLACEMENT_3D('',#49951,#40814,#40815) ;
#32224=AXIS2_PLACEMENT_3D('',#49952,#40816,#40817) ;
#32225=AXIS2_PLACEMENT_3D('',#49961,#40822,#40823) ;
#32226=AXIS2_PLACEMENT_3D('',#49970,#40828,#40829) ;
#32227=AXIS2_PLACEMENT_3D('',#49977,#40834,#40835) ;
#32228=AXIS2_PLACEMENT_3D('',#49981,#40838,#40839) ;
#32229=AXIS2_PLACEMENT_3D('',#49985,#40842,#40843) ;
#32230=AXIS2_PLACEMENT_3D('',#49987,#40845,#40846) ;
#32231=AXIS2_PLACEMENT_3D('',#49989,#40848,#40849) ;
#40807=DIRECTION('axis',(0.,0.,1.)) ;
#40808=DIRECTION('refdir',(1.,0.,0.)) ;
#40809=DIRECTION('center_axis',(0.,0.,1.)) ;
#40810=DIRECTION('ref_axis',(1.,0.,0.)) ;
#40811=DIRECTION('center_axis',(0.,0.,1.)) ;
#40812=DIRECTION('ref_axis',(1.,0.,0.)) ;
#40813=DIRECTION('',(0.,0.,1.)) ;
#40814=DIRECTION('center_axis',(0.,0.,-1.)) ;
#40815=DIRECTION('ref_axis',(1.,0.,0.)) ;
#40816=DIRECTION('center_axis',(-0.5,0.866025403784439,0.)) ;
#40817=DIRECTION('ref_axis',(-0.866025403784439,-0.5,0.)) ;
#40818=DIRECTION('',(0.,0.,1.)) ;
#40819=DIRECTION('',(0.866025403784439,0.5,0.)) ;
#40820=DIRECTION('',(0.,0.,-1.)) ;
#40821=DIRECTION('',(-0.866025403784439,-0.5,0.)) ;
#40822=DIRECTION('center_axis',(0.5,-0.866025403784439,0.)) ;
#40823=DIRECTION('ref_axis',(0.866025403784439,0.5,0.)) ;
#40824=DIRECTION('',(0.,0.,1.)) ;
#40825=DIRECTION('',(-0.866025403784439,-0.5,0.)) ;
#40826=DIRECTION('',(0.,0.,-1.)) ;
#40827=DIRECTION('',(0.866025403784439,0.5,0.)) ;
#40828=DIRECTION('center_axis',(0.,0.,-1.)) ;
#40829=DIRECTION('ref_axis',(-1.,0.,0.)) ;
#40830=DIRECTION('',(0.866025403784439,-0.5,0.)) ;
#40831=DIRECTION('',(0.,-1.,0.)) ;
#40832=DIRECTION('',(-0.866025403784439,0.5,0.)) ;
#40833=DIRECTION('',(0.,1.,0.)) ;
#40834=DIRECTION('center_axis',(0.5,0.866025403784439,0.)) ;
#40835=DIRECTION('ref_axis',(-0.866025403784439,0.5,0.)) ;
#40836=DIRECTION('',(0.,0.,1.)) ;
#40837=DIRECTION('',(-0.866025403784439,0.5,0.)) ;
#40838=DIRECTION('center_axis',(-0.5,-0.866025403784439,0.)) ;
#40839=DIRECTION('ref_axis',(0.866025403784439,-0.5,0.)) ;
#40840=DIRECTION('',(0.,0.,1.)) ;
#40841=DIRECTION('',(0.866025403784439,-0.5,0.)) ;
#40842=DIRECTION('center_axis',(1.,0.,0.)) ;
#40843=DIRECTION('ref_axis',(0.,1.,0.)) ;
#40844=DIRECTION('',(0.,1.,0.)) ;
#40845=DIRECTION('center_axis',(-1.,0.,0.)) ;
#40846=DIRECTION('ref_axis',(0.,-1.,0.)) ;
#40847=DIRECTION('',(0.,-1.,0.)) ;
#40848=DIRECTION('center_axis',(0.,0.,1.)) ;
#40849=DIRECTION('ref_axis',(1.,0.,0.)) ;
#49945=CARTESIAN_POINT('',(0.,0.,0.)) ;
#49946=CARTESIAN_POINT('Origin',(0.,0.,0.)) ;
#49947=CARTESIAN_POINT('',(-0.6,-7.34788079488412E-17,-0.5)) ;
#49948=CARTESIAN_POINT('Origin',(0.,0.,-0.5)) ;
#49949=CARTESIAN_POINT('',(-0.6,7.34788079488412E-17,0.5)) ;
#49950=CARTESIAN_POINT('',(-0.6,-7.34788079488412E-17,0.)) ;
#49951=CARTESIAN_POINT('Origin',(0.,0.,0.5)) ;
#49952=CARTESIAN_POINT('Origin',(0.475,-0.822724133595217,0.)) ;
#49953=CARTESIAN_POINT('',(-2.77555756156289E-16,-1.09696551146029,-0.5)) ;
#49954=CARTESIAN_POINT('',(-2.77555756156289E-16,-1.09696551146029,0.5)) ;
#49955=CARTESIAN_POINT('',(-2.77555756156289E-16,-1.09696551146029,0.)) ;
#49956=CARTESIAN_POINT('',(0.95,-0.548482755730144,-0.5)) ;
#49957=CARTESIAN_POINT('',(0.475,-0.822724133595217,-0.5)) ;
#49958=CARTESIAN_POINT('',(0.95,-0.548482755730144,0.5)) ;
#49959=CARTESIAN_POINT('',(0.95,-0.548482755730144,0.)) ;
#49960=CARTESIAN_POINT('',(0.475,-0.822724133595217,0.5)) ;
#49961=CARTESIAN_POINT('Origin',(-0.475,0.822724133595217,0.)) ;
#49962=CARTESIAN_POINT('',(2.77555756156289E-16,1.09696551146029,-0.5)) ;
#49963=CARTESIAN_POINT('',(2.77555756156289E-16,1.09696551146029,0.5)) ;
#49964=CARTESIAN_POINT('',(2.77555756156289E-16,1.09696551146029,0.)) ;
#49965=CARTESIAN_POINT('',(-0.95,0.548482755730144,-0.5)) ;
#49966=CARTESIAN_POINT('',(-0.475,0.822724133595217,-0.5)) ;
#49967=CARTESIAN_POINT('',(-0.95,0.548482755730144,0.5)) ;
#49968=CARTESIAN_POINT('',(-0.95,0.548482755730144,0.)) ;
#49969=CARTESIAN_POINT('',(-0.475,0.822724133595217,0.5)) ;
#49970=CARTESIAN_POINT('Origin',(0.,0.,-0.5)) ;
#49971=CARTESIAN_POINT('',(-0.95,-0.548482755730144,-0.5)) ;
#49972=CARTESIAN_POINT('',(-0.475,-0.822724133595217,-0.5)) ;
#49973=CARTESIAN_POINT('',(-0.95,0.,-0.5)) ;
#49974=CARTESIAN_POINT('',(0.95,0.548482755730144,-0.5)) ;
#49975=CARTESIAN_POINT('',(0.475,0.822724133595217,-0.5)) ;
#49976=CARTESIAN_POINT('',(0.95,0.,-0.5)) ;
#49977=CARTESIAN_POINT('Origin',(-0.475,-0.822724133595217,0.)) ;
#49978=CARTESIAN_POINT('',(-0.95,-0.548482755730144,0.5)) ;
#49979=CARTESIAN_POINT('',(-0.95,-0.548482755730144,0.)) ;
#49980=CARTESIAN_POINT('',(-0.475,-0.822724133595217,0.5)) ;
#49981=CARTESIAN_POINT('Origin',(0.475,0.822724133595217,0.)) ;
#49982=CARTESIAN_POINT('',(0.95,0.548482755730144,0.5)) ;
#49983=CARTESIAN_POINT('',(0.95,0.548482755730144,0.)) ;
#49984=CARTESIAN_POINT('',(0.475,0.822724133595217,0.5)) ;
#49985=CARTESIAN_POINT('Origin',(-0.95,0.,0.)) ;
#49986=CARTESIAN_POINT('',(-0.95,0.,0.5)) ;
#49987=CARTESIAN_POINT('Origin',(0.95,0.,0.)) ;
#49988=CARTESIAN_POINT('',(0.95,0.,0.5)) ;
#49989=CARTESIAN_POINT('Origin',(0.,0.,0.5)) ;
#50381=UNCERTAINTY_MEASURE_WITH_UNIT(LENGTH_MEASURE(0.001),#50441,
'DISTANCE_ACCURACY_VALUE',
'Maximum model space distance between geometric entities at asserted c
onnectivities') ;
#50387=UNCERTAINTY_MEASURE_WITH_UNIT(LENGTH_MEASURE(0.001),#50441,
'DISTANCE_ACCURACY_VALUE',
'Maximum model space distance between geometric entities at asserted c
onnectivities') ;
#50434=(
GEOMETRIC_REPRESENTATION_CONTEXT(3)
GLOBAL_UNCERTAINTY_ASSIGNED_CONTEXT((#50381))
GLOBAL_UNIT_ASSIGNED_CONTEXT((#50441,#50443,#50444))
REPRESENTATION_CONTEXT('','3D')
) ;
#50440=(
GEOMETRIC_REPRESENTATION_CONTEXT(3)
GLOBAL_UNCERTAINTY_ASSIGNED_CONTEXT((#50387))
GLOBAL_UNIT_ASSIGNED_CONTEXT((#50441,#50443,#50444))
REPRESENTATION_CONTEXT('','3D')
) ;
#50441=(
LENGTH_UNIT()
NAMED_UNIT(*)
SI_UNIT(.CENTI.,.METRE.)
) ;
#50443=(
NAMED_UNIT(*)
PLANE_ANGLE_UNIT()
SI_UNIT($,.RADIAN.)
) ;
#50444=(
NAMED_UNIT(*)
SI_UNIT($,.STERADIAN.)
SOLID_ANGLE_UNIT()
) ;
#50491=SHAPE_DEFINITION_REPRESENTATION(#50587,#50665) ;
#50587=PRODUCT_DEFINITION_SHAPE('',$,#50718) ;
#50665=SHAPE_REPRESENTATION('',(#32220),#50434) ;
#50671=PRODUCT_DEFINITION_CONTEXT('part definition',#50829,'design') ;
#50718=PRODUCT_DEFINITION('GEARBOX_MOUNT_NUT_M12',
'GEARBOX_MOUNT_NUT_M12',#50770,#50671) ;
#50770=PRODUCT_DEFINITION_FORMATION('',$,#50877) ;
#50829=APPLICATION_CONTEXT(
'Core Data for Automotive Mechanical Design Process') ;
#50830=PRODUCT_CONTEXT('part definition',#50829,'mechanical') ;
#50877=PRODUCT('GEARBOX_MOUNT_NUT_M12','GEARBOX_MOUNT_NUT_M12',$,(#50830)) ;
#50883=PRESENTATION_STYLE_ASSIGNMENT((#50890)) ;
#50890=SURFACE_STYLE_USAGE(.BOTH.,#50897) ;
#50897=SURFACE_SIDE_STYLE('',(#50904)) ;
#50904=SURFACE_STYLE_FILL_AREA(#50911) ;
#50911=FILL_AREA_STYLE('Steel - Satin',(#50918)) ;
#50918=FILL_AREA_STYLE_COLOUR('Steel - Satin',#50925) ;
#50925=COLOUR_RGB('Steel - Satin', 0.31764706, 0.68627451, 0.89019608) ;
ENDSEC;
END-ISO-10303-21;
